ISO-10303-21;
HEADER;
/* Generated by software containing ST-Developer
 * from STEP Tools, Inc. (www.steptools.com) 
 */

FILE_DESCRIPTION(
/* description */ ('Crank-driven oscillating fan base (mechanism only)'),

/* implementation_level */ '2;1');

FILE_NAME(
/* name */ 'Rear link spacer (1).step',
/* time_stamp */ '2026-10-28T03:25:00-07:00',
/* author */ (''),
/* organization */ (''),
/* preprocessor_version */ 'ST-DEVELOPER v20.2',
/* originating_system */ 'Autodesk Translation Framework v15.17.0.0',
/* authorisation */ '');

FILE_SCHEMA (('AUTOMOTIVE_DESIGN { 1 0 10303 214 3 1 1 }'));
ENDSEC;

DATA;
#10=MECHANICAL_DESIGN_GEOMETRIC_PRESENTATION_REPRESENTATION('',(#475),#11916);
#387=SHAPE_REPRESENTATION_RELATIONSHIP('SRR','None',#12114,#427);
#427=ADVANCED_BREP_SHAPE_REPRESENTATION('',(#522),#11905);
#475=STYLED_ITEM('',(#12389),#522);
#522=MANIFOLD_SOLID_BREP('Body1',#6106);
#673=FACE_BOUND('',#1706,.T.);
#674=FACE_BOUND('',#1708,.T.);
#839=PLANE('',#7220);
#840=PLANE('',#7221);
#1185=FACE_OUTER_BOUND('',#1703,.T.);
#1186=FACE_OUTER_BOUND('',#1704,.T.);
#1187=FACE_OUTER_BOUND('',#1705,.T.);
#1188=FACE_OUTER_BOUND('',#1707,.T.);
#1703=EDGE_LOOP('',(#5268,#5269,#5270,#5271));
#1704=EDGE_LOOP('',(#5272,#5273,#5274,#5275));
#1705=EDGE_LOOP('',(#5276));
#1706=EDGE_LOOP('',(#5277));
#1707=EDGE_LOOP('',(#5278));
#1708=EDGE_LOOP('',(#5279));
#2042=LINE('',#11451,#2375);
#2043=LINE('',#11457,#2376);
#2375=VECTOR('',#8969,0.305);
#2376=VECTOR('',#8976,0.5);
#2779=CIRCLE('',#7215,0.305);
#2780=CIRCLE('',#7216,0.305);
#2781=CIRCLE('',#7218,0.5);
#2782=CIRCLE('',#7219,0.5);
#3239=VERTEX_POINT('',#11448);
#3240=VERTEX_POINT('',#11450);
#3241=VERTEX_POINT('',#11454);
#3242=VERTEX_POINT('',#11456);
#3929=EDGE_CURVE('',#3239,#3239,#2779,.T.);
#3930=EDGE_CURVE('',#3239,#3240,#2042,.T.);
#3931=EDGE_CURVE('',#3240,#3240,#2780,.T.);
#3932=EDGE_CURVE('',#3241,#3241,#2781,.T.);
#3933=EDGE_CURVE('',#3241,#3242,#2043,.T.);
#3934=EDGE_CURVE('',#3242,#3242,#2782,.T.);
#5268=ORIENTED_EDGE('',*,*,#3929,.F.);
#5269=ORIENTED_EDGE('',*,*,#3930,.T.);
#5270=ORIENTED_EDGE('',*,*,#3931,.T.);
#5271=ORIENTED_EDGE('',*,*,#3930,.F.);
#5272=ORIENTED_EDGE('',*,*,#3932,.F.);
#5273=ORIENTED_EDGE('',*,*,#3933,.T.);
#5274=ORIENTED_EDGE('',*,*,#3934,.T.);
#5275=ORIENTED_EDGE('',*,*,#3933,.F.);
#5276=ORIENTED_EDGE('',*,*,#3932,.T.);
#5277=ORIENTED_EDGE('',*,*,#3929,.T.);
#5278=ORIENTED_EDGE('',*,*,#3934,.F.);
#5279=ORIENTED_EDGE('',*,*,#3931,.F.);
#5671=CYLINDRICAL_SURFACE('',#7214,0.305);
#5672=CYLINDRICAL_SURFACE('',#7217,0.5);
#5991=ADVANCED_FACE('',(#1185),#5671,.F.);
#5992=ADVANCED_FACE('',(#1186),#5672,.T.);
#5993=ADVANCED_FACE('',(#1187,#673),#839,.T.);
#5994=ADVANCED_FACE('',(#1188,#674),#840,.F.);
#6106=CLOSED_SHELL('',(#5991,#5992,#5993,#5994));
#7213=AXIS2_PLACEMENT_3D('',#11446,#8963,#8964);
#7214=AXIS2_PLACEMENT_3D('',#11447,#8965,#8966);
#7215=AXIS2_PLACEMENT_3D('',#11449,#8967,#8968);
#7216=AXIS2_PLACEMENT_3D('',#11452,#8970,#8971);
#7217=AXIS2_PLACEMENT_3D('',#11453,#8972,#8973);
#7218=AXIS2_PLACEMENT_3D('',#11455,#8974,#8975);
#7219=AXIS2_PLACEMENT_3D('',#11458,#8977,#8978);
#7220=AXIS2_PLACEMENT_3D('',#11459,#8979,#8980);
#7221=AXIS2_PLACEMENT_3D('',#11460,#8981,#8982);
#8963=DIRECTION('axis',(0.,0.,1.));
#8964=DIRECTION('refdir',(1.,0.,0.));
#8965=DIRECTION('center_axis',(0.,0.,1.));
#8966=DIRECTION('ref_axis',(1.,0.,0.));
#8967=DIRECTION('center_axis',(0.,0.,-1.));
#8968=DIRECTION('ref_axis',(1.,0.,0.));
#8969=DIRECTION('',(0.,0.,-1.));
#8970=DIRECTION('center_axis',(0.,0.,-1.));
#8971=DIRECTION('ref_axis',(1.,0.,0.));
#8972=DIRECTION('center_axis',(0.,0.,1.));
#8973=DIRECTION('ref_axis',(1.,0.,0.));
#8974=DIRECTION('center_axis',(0.,0.,1.));
#8975=DIRECTION('ref_axis',(1.,0.,0.));
#8976=DIRECTION('',(0.,0.,-1.));
#8977=DIRECTION('center_axis',(0.,0.,1.));
#8978=DIRECTION('ref_axis',(1.,0.,0.));
#8979=DIRECTION('center_axis',(0.,0.,1.));
#8980=DIRECTION('ref_axis',(1.,0.,0.));
#8981=DIRECTION('center_axis',(0.,0.,1.));
#8982=DIRECTION('ref_axis',(1.,0.,0.));
#11446=CARTESIAN_POINT('',(0.,0.,0.));
#11447=CARTESIAN_POINT('Origin',(8.,4.,7.4));
#11448=CARTESIAN_POINT('',(7.695,4.,8.6));
#11449=CARTESIAN_POINT('Origin',(8.,4.,8.6));
#11450=CARTESIAN_POINT('',(7.695,4.,7.4));
#11451=CARTESIAN_POINT('',(7.695,4.,7.4));
#11452=CARTESIAN_POINT('Origin',(8.,4.,7.4));
#11453=CARTESIAN_POINT('Origin',(8.,4.,7.4));
#11454=CARTESIAN_POINT('',(7.5,4.,8.6));
#11455=CARTESIAN_POINT('Origin',(8.,4.,8.6));
#11456=CARTESIAN_POINT('',(7.5,4.,7.4));
#11457=CARTESIAN_POINT('',(7.5,4.,7.4));
#11458=CARTESIAN_POINT('Origin',(8.,4.,7.4));
#11459=CARTESIAN_POINT('Origin',(8.,4.,8.6));
#11460=CARTESIAN_POINT('Origin',(8.,4.,7.4));
#11858=UNCERTAINTY_MEASURE_WITH_UNIT(LENGTH_MEASURE(0.001),#11917,
'DISTANCE_ACCURACY_VALUE',
'Maximum model space distance between geometric entities at asserted c
onnectivities');
#11869=UNCERTAINTY_MEASURE_WITH_UNIT(LENGTH_MEASURE(0.001),#11917,
'DISTANCE_ACCURACY_VALUE',
'Maximum model space distance between geometric entities at asserted c
onnectivities');
#11905=(
GEOMETRIC_REPRESENTATION_CONTEXT(3)
GLOBAL_UNCERTAINTY_ASSIGNED_CONTEXT((#11858))
GLOBAL_UNIT_ASSIGNED_CONTEXT((#11917,#11919,#11920))
REPRESENTATION_CONTEXT('','3D')
);
#11916=(
GEOMETRIC_REPRESENTATION_CONTEXT(3)
GLOBAL_UNCERTAINTY_ASSIGNED_CONTEXT((#11869))
GLOBAL_UNIT_ASSIGNED_CONTEXT((#11917,#11919,#11920))
REPRESENTATION_CONTEXT('','3D')
);
#11917=(
LENGTH_UNIT()
NAMED_UNIT(*)
SI_UNIT(.CENTI.,.METRE.)
);
#11919=(
NAMED_UNIT(*)
PLANE_ANGLE_UNIT()
SI_UNIT($,.RADIAN.)
);
#11920=(
NAMED_UNIT(*)
SI_UNIT($,.STERADIAN.)
SOLID_ANGLE_UNIT()
);
#11956=SHAPE_DEFINITION_REPRESENTATION(#12007,#12114);
#12007=PRODUCT_DEFINITION_SHAPE('',$,#12161);
#12114=SHAPE_REPRESENTATION('',(#7213),#11905);
#12125=PRODUCT_DEFINITION_CONTEXT('part definition',#12265,'design');
#12161=PRODUCT_DEFINITION('Rear link spacer (1)','Rear link spacer (1)',#12207,
#12125);
#12207=PRODUCT_DEFINITION_FORMATION('',$,#12302);
#12265=APPLICATION_CONTEXT(
'Core Data for Automotive Mechanical Design Process');
#12266=PRODUCT_CONTEXT('part definition',#12265,'mechanical');
#12302=PRODUCT('Rear link spacer (1)','Rear link spacer (1)',
'Rear link spacer (1)',(#12266));
#12383=COLOUR_RGB('Off White',0.89,0.88,0.83);
#12384=FILL_AREA_STYLE_COLOUR('',#12383);
#12385=FILL_AREA_STYLE('',(#12384));
#12386=SURFACE_STYLE_FILL_AREA(#12385);
#12387=SURFACE_SIDE_STYLE('',(#12386));
#12388=SURFACE_STYLE_USAGE(.BOTH.,#12387);
#12389=PRESENTATION_STYLE_ASSIGNMENT((#12388));
ENDSEC;
END-ISO-10303-21;
